ISO-10303-21;
HEADER;
/* Generated by software containing ST-Developer
 * from STEP Tools, Inc. (www.steptools.com) 
 */

FILE_DESCRIPTION(
/* description */ ('Lever-operated bar clamp (toggle)'),
/* implementation_level */ '2;1');

FILE_NAME(
/* name */ 'M4x30 stop screw.step',
/* time_stamp */ '2026-10-28T03:25:02-07:00',
/* author */ (''),
/* organization */ (''),
/* preprocessor_version */ 'ST-DEVELOPER v20.2',
/* originating_system */ 'Autodesk Translation Framework v15.17.0.0',
/* authorisation */ '');

FILE_SCHEMA (('AUTOMOTIVE_DESIGN { 1 0 10303 214 3 1 1 }'));
ENDSEC;

DATA;
#10=MECHANICAL_DESIGN_GEOMETRIC_PRESENTATION_REPRESENTATION('',(#437),#12413);
#312=CONICAL_SURFACE('',#7530,0.325,0.785398163397448);
#313=CONICAL_SURFACE('',#7534,0.335,0.785398163397448);
#314=CONICAL_SURFACE('',#7538,0.21,0.463647609000806);
#315=CONICAL_SURFACE('',#7542,0.18,0.785398163397448);
#327=ORIENTED_CLOSED_SHELL('',*,#6597,.F.);
#331=BREP_WITH_VOIDS('Body1',#6598,(#327));
#353=SHAPE_REPRESENTATION_RELATIONSHIP('SRR','None',#12594,#391);
#391=ADVANCED_BREP_SHAPE_REPRESENTATION('',(#331),#12391);
#437=STYLED_ITEM('',(#12876),#331);
#608=FACE_BOUND('',#1638,.T.);
#609=FACE_BOUND('',#1646,.T.);
#773=PLANE('',#7514);
#774=PLANE('',#7515);
#775=PLANE('',#7516);
#776=PLANE('',#7517);
#777=PLANE('',#7518);
#778=PLANE('',#7519);
#779=PLANE('',#7520);
#780=PLANE('',#7521);
#781=PLANE('',#7522);
#782=PLANE('',#7527);
#783=PLANE('',#7528);
#784=PLANE('',#7536);
#1115=FACE_OUTER_BOUND('',#1629,.T.);
#1116=FACE_OUTER_BOUND('',#1630,.T.);
#1117=FACE_OUTER_BOUND('',#1631,.T.);
#1118=FACE_OUTER_BOUND('',#1632,.T.);
#1119=FACE_OUTER_BOUND('',#1633,.T.);
#1120=FACE_OUTER_BOUND('',#1634,.T.);
#1121=FACE_OUTER_BOUND('',#1635,.T.);
#1122=FACE_OUTER_BOUND('',#1636,.T.);
#1123=FACE_OUTER_BOUND('',#1637,.T.);
#1124=FACE_OUTER_BOUND('',#1639,.T.);
#1125=FACE_OUTER_BOUND('',#1640,.T.);
#1126=FACE_OUTER_BOUND('',#1641,.T.);
#1127=FACE_OUTER_BOUND('',#1642,.T.);
#1128=FACE_OUTER_BOUND('',#1643,.T.);
#1129=FACE_OUTER_BOUND('',#1644,.T.);
#1130=FACE_OUTER_BOUND('',#1645,.T.);
#1131=FACE_OUTER_BOUND('',#1647,.T.);
#1132=FACE_OUTER_BOUND('',#1648,.T.);
#1133=FACE_OUTER_BOUND('',#1649,.T.);
#1629=EDGE_LOOP('',(#5353,#5354,#5355,#5356));
#1630=EDGE_LOOP('',(#5357,#5358,#5359,#5360));
#1631=EDGE_LOOP('',(#5361,#5362,#5363,#5364));
#1632=EDGE_LOOP('',(#5365,#5366,#5367,#5368));
#1633=EDGE_LOOP('',(#5369,#5370,#5371,#5372));
#1634=EDGE_LOOP('',(#5373,#5374,#5375,#5376));
#1635=EDGE_LOOP('',(#5377,#5378,#5379,#5380,#5381,#5382));
#1636=EDGE_LOOP('',(#5383,#5384,#5385,#5386,#5387,#5388));
#1637=EDGE_LOOP('',(#5389));
#1638=EDGE_LOOP('',(#5390));
#1639=EDGE_LOOP('',(#5391,#5392,#5393,#5394));
#1640=EDGE_LOOP('',(#5395));
#1641=EDGE_LOOP('',(#5396));
#1642=EDGE_LOOP('',(#5397,#5398,#5399,#5400));
#1643=EDGE_LOOP('',(#5401,#5402,#5403,#5404));
#1644=EDGE_LOOP('',(#5405,#5406,#5407,#5408));
#1645=EDGE_LOOP('',(#5409));
#1646=EDGE_LOOP('',(#5410));
#1647=EDGE_LOOP('',(#5411,#5412,#5413,#5414));
#1648=EDGE_LOOP('',(#5415,#5416,#5417,#5418));
#1649=EDGE_LOOP('',(#5419,#5420,#5421,#5422));
#2082=LINE('',#11429,#2523);
#2083=LINE('',#11431,#2524);
#2084=LINE('',#11433,#2525);
#2085=LINE('',#11434,#2526);
#2086=LINE('',#11437,#2527);
#2087=LINE('',#11439,#2528);
#2088=LINE('',#11440,#2529);
#2089=LINE('',#11443,#2530);
#2090=LINE('',#11445,#2531);
#2091=LINE('',#11446,#2532);
#2092=LINE('',#11449,#2533);
#2093=LINE('',#11451,#2534);
#2094=LINE('',#11452,#2535);
#2095=LINE('',#11455,#2536);
#2096=LINE('',#11457,#2537);
#2097=LINE('',#11458,#2538);
#2098=LINE('',#11460,#2539);
#2099=LINE('',#11461,#2540);
#2100=LINE('',#11471,#2541);
#2101=LINE('',#11480,#2542);
#2102=LINE('',#11484,#2543);
#2103=LINE('',#11488,#2544);
#2104=LINE('',#11495,#2545);
#2105=LINE('',#11499,#2546);
#2106=LINE('',#11501,#2547);
#2523=VECTOR('',#9077,1.);
#2524=VECTOR('',#9078,1.);
#2525=VECTOR('',#9079,1.);
#2526=VECTOR('',#9080,1.);
#2527=VECTOR('',#9083,1.);
#2528=VECTOR('',#9084,1.);
#2529=VECTOR('',#9085,1.);
#2530=VECTOR('',#9088,1.);
#2531=VECTOR('',#9089,1.);
#2532=VECTOR('',#9090,1.);
#2533=VECTOR('',#9093,1.);
#2534=VECTOR('',#9094,1.);
#2535=VECTOR('',#9095,1.);
#2536=VECTOR('',#9098,1.);
#2537=VECTOR('',#9099,1.);
#2538=VECTOR('',#9100,1.);
#2539=VECTOR('',#9103,1.);
#2540=VECTOR('',#9104,1.);
#2541=VECTOR('',#9117,0.2);
#2542=VECTOR('',#9130,0.325);
#2543=VECTOR('',#9135,0.35);
#2544=VECTOR('',#9140,0.335);
#2545=VECTOR('',#9149,0.21);
#2546=VECTOR('',#9154,0.2);
#2547=VECTOR('',#9157,0.18);
#2950=CIRCLE('',#7523,0.2);
#2951=CIRCLE('',#7524,0.16);
#2952=CIRCLE('',#7526,0.2);
#2953=CIRCLE('',#7529,0.3);
#2954=CIRCLE('',#7531,0.35);
#2955=CIRCLE('',#7533,0.35);
#2956=CIRCLE('',#7535,0.32);
#2957=CIRCLE('',#7537,0.22);
#2958=CIRCLE('',#7539,0.1954);
#2959=CIRCLE('',#7541,0.1954);
#3393=VERTEX_POINT('',#11427);
#3394=VERTEX_POINT('',#11428);
#3395=VERTEX_POINT('',#11430);
#3396=VERTEX_POINT('',#11432);
#3397=VERTEX_POINT('',#11436);
#3398=VERTEX_POINT('',#11438);
#3399=VERTEX_POINT('',#11442);
#3400=VERTEX_POINT('',#11444);
#3401=VERTEX_POINT('',#11448);
#3402=VERTEX_POINT('',#11450);
#3403=VERTEX_POINT('',#11454);
#3404=VERTEX_POINT('',#11456);
#3405=VERTEX_POINT('',#11465);
#3406=VERTEX_POINT('',#11467);
#3407=VERTEX_POINT('',#11470);
#3408=VERTEX_POINT('',#11475);
#3409=VERTEX_POINT('',#11478);
#3410=VERTEX_POINT('',#11482);
#3411=VERTEX_POINT('',#11486);
#3412=VERTEX_POINT('',#11490);
#3413=VERTEX_POINT('',#11493);
#3414=VERTEX_POINT('',#11497);
#4081=EDGE_CURVE('',#3393,#3394,#2082,.T.);
#4082=EDGE_CURVE('',#3394,#3395,#2083,.T.);
#4083=EDGE_CURVE('',#3395,#3396,#2084,.T.);
#4084=EDGE_CURVE('',#3393,#3396,#2085,.T.);
#4085=EDGE_CURVE('',#3394,#3397,#2086,.T.);
#4086=EDGE_CURVE('',#3397,#3398,#2087,.T.);
#4087=EDGE_CURVE('',#3398,#3395,#2088,.T.);
#4088=EDGE_CURVE('',#3397,#3399,#2089,.T.);
#4089=EDGE_CURVE('',#3399,#3400,#2090,.T.);
#4090=EDGE_CURVE('',#3400,#3398,#2091,.T.);
#4091=EDGE_CURVE('',#3399,#3401,#2092,.T.);
#4092=EDGE_CURVE('',#3401,#3402,#2093,.T.);
#4093=EDGE_CURVE('',#3402,#3400,#2094,.T.);
#4094=EDGE_CURVE('',#3401,#3403,#2095,.T.);
#4095=EDGE_CURVE('',#3403,#3404,#2096,.T.);
#4096=EDGE_CURVE('',#3404,#3402,#2097,.T.);
#4097=EDGE_CURVE('',#3403,#3393,#2098,.T.);
#4098=EDGE_CURVE('',#3396,#3404,#2099,.T.);
#4099=EDGE_CURVE('',#3405,#3405,#2950,.T.);
#4100=EDGE_CURVE('',#3406,#3406,#2951,.T.);
#4101=EDGE_CURVE('',#3405,#3407,#2100,.T.);
#4102=EDGE_CURVE('',#3407,#3407,#2952,.T.);
#4103=EDGE_CURVE('',#3408,#3408,#2953,.T.);
#4104=EDGE_CURVE('',#3409,#3409,#2954,.T.);
#4105=EDGE_CURVE('',#3409,#3408,#2101,.T.);
#4106=EDGE_CURVE('',#3410,#3410,#2955,.T.);
#4107=EDGE_CURVE('',#3410,#3409,#2102,.T.);
#4108=EDGE_CURVE('',#3411,#3411,#2956,.T.);
#4109=EDGE_CURVE('',#3411,#3410,#2103,.T.);
#4110=EDGE_CURVE('',#3412,#3412,#2957,.T.);
#4111=EDGE_CURVE('',#3413,#3413,#2958,.F.);
#4112=EDGE_CURVE('',#3413,#3412,#2104,.T.);
#4113=EDGE_CURVE('',#3414,#3414,#2959,.F.);
#4114=EDGE_CURVE('',#3414,#3413,#2105,.T.);
#4115=EDGE_CURVE('',#3406,#3414,#2106,.T.);
#5353=ORIENTED_EDGE('',*,*,#4081,.T.);
#5354=ORIENTED_EDGE('',*,*,#4082,.T.);
#5355=ORIENTED_EDGE('',*,*,#4083,.T.);
#5356=ORIENTED_EDGE('',*,*,#4084,.F.);
#5357=ORIENTED_EDGE('',*,*,#4085,.T.);
#5358=ORIENTED_EDGE('',*,*,#4086,.T.);
#5359=ORIENTED_EDGE('',*,*,#4087,.T.);
#5360=ORIENTED_EDGE('',*,*,#4082,.F.);
#5361=ORIENTED_EDGE('',*,*,#4088,.T.);
#5362=ORIENTED_EDGE('',*,*,#4089,.T.);
#5363=ORIENTED_EDGE('',*,*,#4090,.T.);
#5364=ORIENTED_EDGE('',*,*,#4086,.F.);
#5365=ORIENTED_EDGE('',*,*,#4091,.T.);
#5366=ORIENTED_EDGE('',*,*,#4092,.T.);
#5367=ORIENTED_EDGE('',*,*,#4093,.T.);
#5368=ORIENTED_EDGE('',*,*,#4089,.F.);
#5369=ORIENTED_EDGE('',*,*,#4094,.T.);
#5370=ORIENTED_EDGE('',*,*,#4095,.T.);
#5371=ORIENTED_EDGE('',*,*,#4096,.T.);
#5372=ORIENTED_EDGE('',*,*,#4092,.F.);
#5373=ORIENTED_EDGE('',*,*,#4097,.T.);
#5374=ORIENTED_EDGE('',*,*,#4084,.T.);
#5375=ORIENTED_EDGE('',*,*,#4098,.T.);
#5376=ORIENTED_EDGE('',*,*,#4095,.F.);
#5377=ORIENTED_EDGE('',*,*,#4097,.F.);
#5378=ORIENTED_EDGE('',*,*,#4094,.F.);
#5379=ORIENTED_EDGE('',*,*,#4091,.F.);
#5380=ORIENTED_EDGE('',*,*,#4088,.F.);
#5381=ORIENTED_EDGE('',*,*,#4085,.F.);
#5382=ORIENTED_EDGE('',*,*,#4081,.F.);
#5383=ORIENTED_EDGE('',*,*,#4098,.F.);
#5384=ORIENTED_EDGE('',*,*,#4083,.F.);
#5385=ORIENTED_EDGE('',*,*,#4087,.F.);
#5386=ORIENTED_EDGE('',*,*,#4090,.F.);
#5387=ORIENTED_EDGE('',*,*,#4093,.F.);
#5388=ORIENTED_EDGE('',*,*,#4096,.F.);
#5389=ORIENTED_EDGE('',*,*,#4099,.T.);
#5390=ORIENTED_EDGE('',*,*,#4100,.T.);
#5391=ORIENTED_EDGE('',*,*,#4099,.F.);
#5392=ORIENTED_EDGE('',*,*,#4101,.T.);
#5393=ORIENTED_EDGE('',*,*,#4102,.T.);
#5394=ORIENTED_EDGE('',*,*,#4101,.F.);
#5395=ORIENTED_EDGE('',*,*,#4102,.F.);
#5396=ORIENTED_EDGE('',*,*,#4103,.F.);
#5397=ORIENTED_EDGE('',*,*,#4104,.F.);
#5398=ORIENTED_EDGE('',*,*,#4105,.T.);
#5399=ORIENTED_EDGE('',*,*,#4103,.T.);
#5400=ORIENTED_EDGE('',*,*,#4105,.F.);
#5401=ORIENTED_EDGE('',*,*,#4106,.F.);
#5402=ORIENTED_EDGE('',*,*,#4107,.T.);
#5403=ORIENTED_EDGE('',*,*,#4104,.T.);
#5404=ORIENTED_EDGE('',*,*,#4107,.F.);
#5405=ORIENTED_EDGE('',*,*,#4108,.F.);
#5406=ORIENTED_EDGE('',*,*,#4109,.T.);
#5407=ORIENTED_EDGE('',*,*,#4106,.T.);
#5408=ORIENTED_EDGE('',*,*,#4109,.F.);
#5409=ORIENTED_EDGE('',*,*,#4108,.T.);
#5410=ORIENTED_EDGE('',*,*,#4110,.F.);
#5411=ORIENTED_EDGE('',*,*,#4111,.F.);
#5412=ORIENTED_EDGE('',*,*,#4112,.T.);
#5413=ORIENTED_EDGE('',*,*,#4110,.T.);
#5414=ORIENTED_EDGE('',*,*,#4112,.F.);
#5415=ORIENTED_EDGE('',*,*,#4113,.F.);
#5416=ORIENTED_EDGE('',*,*,#4114,.T.);
#5417=ORIENTED_EDGE('',*,*,#4111,.T.);
#5418=ORIENTED_EDGE('',*,*,#4114,.F.);
#5419=ORIENTED_EDGE('',*,*,#4100,.F.);
#5420=ORIENTED_EDGE('',*,*,#4115,.T.);
#5421=ORIENTED_EDGE('',*,*,#4113,.T.);
#5422=ORIENTED_EDGE('',*,*,#4115,.F.);
#6113=CYLINDRICAL_SURFACE('',#7525,0.2);
#6114=CYLINDRICAL_SURFACE('',#7532,0.35);
#6115=CYLINDRICAL_SURFACE('',#7540,0.1954);
#6390=ADVANCED_FACE('',(#1115),#773,.F.);
#6391=ADVANCED_FACE('',(#1116),#774,.F.);
#6392=ADVANCED_FACE('',(#1117),#775,.F.);
#6393=ADVANCED_FACE('',(#1118),#776,.F.);
#6394=ADVANCED_FACE('',(#1119),#777,.F.);
#6395=ADVANCED_FACE('',(#1120),#778,.F.);
#6396=ADVANCED_FACE('',(#1121),#779,.F.);
#6397=ADVANCED_FACE('',(#1122),#780,.F.);
#6398=ADVANCED_FACE('',(#1123,#608),#781,.T.);
#6399=ADVANCED_FACE('',(#1124),#6113,.T.);
#6400=ADVANCED_FACE('',(#1125),#782,.F.);
#6401=ADVANCED_FACE('',(#1126),#783,.T.);
#6402=ADVANCED_FACE('',(#1127),#312,.T.);
#6403=ADVANCED_FACE('',(#1128),#6114,.T.);
#6404=ADVANCED_FACE('',(#1129),#313,.T.);
#6405=ADVANCED_FACE('',(#1130,#609),#784,.T.);
#6406=ADVANCED_FACE('',(#1131),#314,.T.);
#6407=ADVANCED_FACE('',(#1132),#6115,.T.);
#6408=ADVANCED_FACE('',(#1133),#315,.T.);
#6597=CLOSED_SHELL('',(#6390,#6391,#6392,#6393,#6394,#6395,#6396,#6397));
#6598=CLOSED_SHELL('',(#6398,#6399,#6400,#6401,#6402,#6403,#6404,#6405,
#6406,#6407,#6408));
#7513=AXIS2_PLACEMENT_3D('',#11425,#9073,#9074);
#7514=AXIS2_PLACEMENT_3D('',#11426,#9075,#9076);
#7515=AXIS2_PLACEMENT_3D('',#11435,#9081,#9082);
#7516=AXIS2_PLACEMENT_3D('',#11441,#9086,#9087);
#7517=AXIS2_PLACEMENT_3D('',#11447,#9091,#9092);
#7518=AXIS2_PLACEMENT_3D('',#11453,#9096,#9097);
#7519=AXIS2_PLACEMENT_3D('',#11459,#9101,#9102);
#7520=AXIS2_PLACEMENT_3D('',#11462,#9105,#9106);
#7521=AXIS2_PLACEMENT_3D('',#11463,#9107,#9108);
#7522=AXIS2_PLACEMENT_3D('',#11464,#9109,#9110);
#7523=AXIS2_PLACEMENT_3D('',#11466,#9111,#9112);
#7524=AXIS2_PLACEMENT_3D('',#11468,#9113,#9114);
#7525=AXIS2_PLACEMENT_3D('',#11469,#9115,#9116);
#7526=AXIS2_PLACEMENT_3D('',#11472,#9118,#9119);
#7527=AXIS2_PLACEMENT_3D('',#11473,#9120,#9121);
#7528=AXIS2_PLACEMENT_3D('',#11474,#9122,#9123);
#7529=AXIS2_PLACEMENT_3D('',#11476,#9124,#9125);
#7530=AXIS2_PLACEMENT_3D('',#11477,#9126,#9127);
#7531=AXIS2_PLACEMENT_3D('',#11479,#9128,#9129);
#7532=AXIS2_PLACEMENT_3D('',#11481,#9131,#9132);
#7533=AXIS2_PLACEMENT_3D('',#11483,#9133,#9134);
#7534=AXIS2_PLACEMENT_3D('',#11485,#9136,#9137);
#7535=AXIS2_PLACEMENT_3D('',#11487,#9138,#9139);
#7536=AXIS2_PLACEMENT_3D('',#11489,#9141,#9142);
#7537=AXIS2_PLACEMENT_3D('',#11491,#9143,#9144);
#7538=AXIS2_PLACEMENT_3D('',#11492,#9145,#9146);
#7539=AXIS2_PLACEMENT_3D('',#11494,#9147,#9148);
#7540=AXIS2_PLACEMENT_3D('',#11496,#9150,#9151);
#7541=AXIS2_PLACEMENT_3D('',#11498,#9152,#9153);
#7542=AXIS2_PLACEMENT_3D('',#11500,#9155,#9156);
#9073=DIRECTION('axis',(0.,0.,1.));
#9074=DIRECTION('refdir',(1.,0.,0.));
#9075=DIRECTION('center_axis',(0.866025403784439,0.,-0.5));
#9076=DIRECTION('ref_axis',(0.5,0.,0.866025403784439));
#9077=DIRECTION('',(-0.5,0.,-0.866025403784439));
#9078=DIRECTION('',(0.,-1.,0.));
#9079=DIRECTION('',(0.5,0.,0.866025403784439));
#9080=DIRECTION('',(0.,-1.,0.));
#9081=DIRECTION('center_axis',(1.60246890531964E-16,0.,-1.));
#9082=DIRECTION('ref_axis',(1.,0.,1.60246890531964E-16));
#9083=DIRECTION('',(-1.,0.,-1.60246890531964E-16));
#9084=DIRECTION('',(0.,-1.,0.));
#9085=DIRECTION('',(1.,0.,1.60246890531964E-16));
#9086=DIRECTION('center_axis',(-0.866025403784439,0.,-0.5));
#9087=DIRECTION('ref_axis',(0.5,0.,-0.866025403784439));
#9088=DIRECTION('',(-0.5,0.,0.866025403784439));
#9089=DIRECTION('',(0.,-1.,0.));
#9090=DIRECTION('',(0.5,0.,-0.866025403784439));
#9091=DIRECTION('center_axis',(-0.866025403784439,0.,0.5));
#9092=DIRECTION('ref_axis',(-0.5,0.,-0.866025403784439));
#9093=DIRECTION('',(0.5,0.,0.866025403784439));
#9094=DIRECTION('',(0.,-1.,0.));
#9095=DIRECTION('',(-0.5,0.,-0.866025403784439));
#9096=DIRECTION('center_axis',(-1.60246890531964E-16,0.,1.));
#9097=DIRECTION('ref_axis',(-1.,0.,-1.60246890531964E-16));
#9098=DIRECTION('',(1.,0.,1.60246890531964E-16));
#9099=DIRECTION('',(0.,-1.,0.));
#9100=DIRECTION('',(-1.,0.,-1.60246890531964E-16));
#9101=DIRECTION('center_axis',(0.866025403784439,0.,0.5));
#9102=DIRECTION('ref_axis',(-0.5,0.,0.866025403784439));
#9103=DIRECTION('',(0.5,0.,-0.866025403784439));
#9104=DIRECTION('',(-0.5,0.,0.866025403784439));
#9105=DIRECTION('center_axis',(0.,1.,0.));
#9106=DIRECTION('ref_axis',(1.,0.,0.));
#9107=DIRECTION('center_axis',(0.,-1.,0.));
#9108=DIRECTION('ref_axis',(0.,0.,-1.));
#9109=DIRECTION('center_axis',(0.,1.,0.));
#9110=DIRECTION('ref_axis',(1.,0.,0.));
#9111=DIRECTION('center_axis',(0.,1.,0.));
#9112=DIRECTION('ref_axis',(1.,0.,0.));
#9113=DIRECTION('center_axis',(0.,-1.,0.));
#9114=DIRECTION('ref_axis',(1.,0.,0.));
#9115=DIRECTION('center_axis',(0.,1.,0.));
#9116=DIRECTION('ref_axis',(1.,0.,0.));
#9117=DIRECTION('',(0.,-1.,0.));
#9118=DIRECTION('center_axis',(0.,1.,0.));
#9119=DIRECTION('ref_axis',(1.,0.,0.));
#9120=DIRECTION('center_axis',(0.,1.,0.));
#9121=DIRECTION('ref_axis',(1.,0.,0.));
#9122=DIRECTION('center_axis',(0.,1.,0.));
#9123=DIRECTION('ref_axis',(0.,0.,1.));
#9124=DIRECTION('center_axis',(0.,-1.,0.));
#9125=DIRECTION('ref_axis',(1.,0.,0.));
#9126=DIRECTION('center_axis',(0.,-1.,0.));
#9127=DIRECTION('ref_axis',(1.,0.,0.));
#9128=DIRECTION('center_axis',(0.,-1.,0.));
#9129=DIRECTION('ref_axis',(1.,0.,0.));
#9130=DIRECTION('',(0.707106781186547,0.707106781186548,8.65956056235493E-17));
#9131=DIRECTION('center_axis',(0.,-1.,0.));
#9132=DIRECTION('ref_axis',(1.,0.,0.));
#9133=DIRECTION('center_axis',(0.,-1.,0.));
#9134=DIRECTION('ref_axis',(1.,0.,0.));
#9135=DIRECTION('',(0.,1.,0.));
#9136=DIRECTION('center_axis',(0.,1.,0.));
#9137=DIRECTION('ref_axis',(1.,0.,0.));
#9138=DIRECTION('center_axis',(0.,-1.,0.));
#9139=DIRECTION('ref_axis',(1.,0.,0.));
#9140=DIRECTION('',(-0.707106781186547,0.707106781186548,-8.65956056235493E-17));
#9141=DIRECTION('center_axis',(0.,-1.,0.));
#9142=DIRECTION('ref_axis',(0.,0.,-1.));
#9143=DIRECTION('center_axis',(0.,-1.,0.));
#9144=DIRECTION('ref_axis',(1.,0.,0.));
#9145=DIRECTION('center_axis',(0.,1.,0.));
#9146=DIRECTION('ref_axis',(1.,0.,0.));
#9147=DIRECTION('center_axis',(0.,1.,0.));
#9148=DIRECTION('ref_axis',(1.,0.,0.));
#9149=DIRECTION('',(-0.447213595499958,0.894427190999916,-5.47678698264203E-17));
#9150=DIRECTION('center_axis',(0.,-1.,0.));
#9151=DIRECTION('ref_axis',(1.,0.,0.));
#9152=DIRECTION('center_axis',(0.,1.,0.));
#9153=DIRECTION('ref_axis',(1.,0.,0.));
#9154=DIRECTION('',(0.,1.,0.));
#9155=DIRECTION('center_axis',(0.,1.,0.));
#9156=DIRECTION('ref_axis',(1.,0.,0.));
#9157=DIRECTION('',(-0.707106781186547,0.707106781186548,-8.65956056235493E-17));
#11425=CARTESIAN_POINT('',(0.,0.,0.));
#11426=CARTESIAN_POINT('Origin',(0.0866025403784439,-0.4,-0.15));
#11427=CARTESIAN_POINT('',(0.173205080756888,-0.4,0.));
#11428=CARTESIAN_POINT('',(0.0866025403784439,-0.4,-0.15));
#11429=CARTESIAN_POINT('',(0.173205080756888,-0.4,0.));
#11430=CARTESIAN_POINT('',(0.0866025403784439,-0.64,-0.15));
#11431=CARTESIAN_POINT('',(0.0866025403784439,-0.4,-0.15));
#11432=CARTESIAN_POINT('',(0.173205080756888,-0.64,0.));
#11433=CARTESIAN_POINT('',(0.173205080756888,-0.64,0.));
#11434=CARTESIAN_POINT('',(0.173205080756888,-0.4,0.));
#11435=CARTESIAN_POINT('Origin',(-0.0866025403784438,-0.4,-0.15));
#11436=CARTESIAN_POINT('',(-0.0866025403784438,-0.4,-0.15));
#11437=CARTESIAN_POINT('',(0.0866025403784439,-0.4,-0.15));
#11438=CARTESIAN_POINT('',(-0.0866025403784438,-0.64,-0.15));
#11439=CARTESIAN_POINT('',(-0.0866025403784438,-0.4,-0.15));
#11440=CARTESIAN_POINT('',(0.0866025403784439,-0.64,-0.15));
#11441=CARTESIAN_POINT('Origin',(-0.173205080756888,-0.4,-2.77555756156289E-17));
#11442=CARTESIAN_POINT('',(-0.173205080756888,-0.4,-2.12115047744981E-17));
#11443=CARTESIAN_POINT('',(-0.0866025403784438,-0.4,-0.15));
#11444=CARTESIAN_POINT('',(-0.173205080756888,-0.64,-2.77555756156289E-17));
#11445=CARTESIAN_POINT('',(-0.173205080756888,-0.4,-2.12115047744981E-17));
#11446=CARTESIAN_POINT('',(-0.0866025403784438,-0.64,-0.15));
#11447=CARTESIAN_POINT('Origin',(-0.0866025403784439,-0.4,0.15));
#11448=CARTESIAN_POINT('',(-0.0866025403784439,-0.4,0.15));
#11449=CARTESIAN_POINT('',(-0.173205080756888,-0.4,-2.12115047744981E-17));
#11450=CARTESIAN_POINT('',(-0.0866025403784439,-0.64,0.15));
#11451=CARTESIAN_POINT('',(-0.0866025403784439,-0.4,0.15));
#11452=CARTESIAN_POINT('',(-0.173205080756888,-0.64,-2.12115047744981E-17));
#11453=CARTESIAN_POINT('Origin',(0.0866025403784439,-0.4,0.15));
#11454=CARTESIAN_POINT('',(0.0866025403784439,-0.4,0.15));
#11455=CARTESIAN_POINT('',(-0.0866025403784439,-0.4,0.15));
#11456=CARTESIAN_POINT('',(0.0866025403784439,-0.64,0.15));
#11457=CARTESIAN_POINT('',(0.0866025403784439,-0.4,0.15));
#11458=CARTESIAN_POINT('',(-0.0866025403784439,-0.64,0.15));
#11459=CARTESIAN_POINT('Origin',(0.173205080756888,-0.4,0.));
#11460=CARTESIAN_POINT('',(0.0866025403784439,-0.4,0.15));
#11461=CARTESIAN_POINT('',(0.0866025403784439,-0.64,0.15));
#11462=CARTESIAN_POINT('Origin',(0.,-0.4,-2.77555756156289E-17));
#11463=CARTESIAN_POINT('Origin',(0.,-0.64,-2.77555756156289E-17));
#11464=CARTESIAN_POINT('Origin',(0.,-1.6,0.));
#11465=CARTESIAN_POINT('',(-0.2,-1.6,2.44929359829471E-17));
#11466=CARTESIAN_POINT('Origin',(0.,-1.6,0.));
#11467=CARTESIAN_POINT('',(-0.16,-1.6,-1.95943487863577E-17));
#11468=CARTESIAN_POINT('Origin',(0.,-1.6,0.));
#11469=CARTESIAN_POINT('Origin',(0.,-3.,0.));
#11470=CARTESIAN_POINT('',(-0.2,-3.,2.44929359829471E-17));
#11471=CARTESIAN_POINT('',(-0.2,-3.,2.44929359829471E-17));
#11472=CARTESIAN_POINT('Origin',(0.,-3.,0.));
#11473=CARTESIAN_POINT('Origin',(0.,-3.,0.));
#11474=CARTESIAN_POINT('Origin',(0.3,0.4,0.));
#11475=CARTESIAN_POINT('',(-0.3,0.4,-3.67394039744206E-17));
#11476=CARTESIAN_POINT('Origin',(0.,0.4,0.));
#11477=CARTESIAN_POINT('Origin',(0.,0.375,0.));
#11478=CARTESIAN_POINT('',(-0.35,0.35,-4.28626379701573E-17));
#11479=CARTESIAN_POINT('Origin',(0.,0.35,0.));
#11480=CARTESIAN_POINT('',(-0.325,0.375,-3.9801020972289E-17));
#11481=CARTESIAN_POINT('Origin',(0.,0.19,0.));
#11482=CARTESIAN_POINT('',(-0.35,0.03,-4.28626379701574E-17));
#11483=CARTESIAN_POINT('Origin',(0.,0.03,0.));
#11484=CARTESIAN_POINT('',(-0.35,0.19,-4.28626379701574E-17));
#11485=CARTESIAN_POINT('Origin',(0.,0.0149999999999999,0.));
#11486=CARTESIAN_POINT('',(-0.32,-3.29597460435593E-17,-3.91886975727153E-17));
#11487=CARTESIAN_POINT('Origin',(0.,0.,0.));
#11488=CARTESIAN_POINT('',(-0.335,0.0149999999999999,-4.10256677714363E-17));
#11489=CARTESIAN_POINT('Origin',(0.22,0.,0.));
#11490=CARTESIAN_POINT('',(-0.22,-6.93889390390723E-18,-2.69422295812418E-17));
#11491=CARTESIAN_POINT('Origin',(0.,0.,0.));
#11492=CARTESIAN_POINT('Origin',(0.,-0.02,0.));
#11493=CARTESIAN_POINT('',(-0.1954,-0.0492,2.39295984553393E-17));
#11494=CARTESIAN_POINT('Origin',(0.,-0.0492,0.));
#11495=CARTESIAN_POINT('',(-0.21,-0.02,-2.57175827820944E-17));
#11496=CARTESIAN_POINT('Origin',(0.,-0.8,0.));
#11497=CARTESIAN_POINT('',(-0.1954,-1.5646,2.39295984553393E-17));
#11498=CARTESIAN_POINT('Origin',(0.,-1.5646,0.));
#11499=CARTESIAN_POINT('',(-0.1954,-0.8,-2.39295984553393E-17));
#11500=CARTESIAN_POINT('Origin',(0.,-1.58,0.));
#11501=CARTESIAN_POINT('',(-0.18,-1.58,-2.20436423846524E-17));
#12345=UNCERTAINTY_MEASURE_WITH_UNIT(LENGTH_MEASURE(0.001),#12414,
'DISTANCE_ACCURACY_VALUE',
'Maximum model space distance between geometric entities at asserted c
onnectivities');
#12367=UNCERTAINTY_MEASURE_WITH_UNIT(LENGTH_MEASURE(0.001),#12414,
'DISTANCE_ACCURACY_VALUE',
'Maximum model space distance between geometric entities at asserted c
onnectivities');
#12391=(
GEOMETRIC_REPRESENTATION_CONTEXT(3)
GLOBAL_UNCERTAINTY_ASSIGNED_CONTEXT((#12345))
GLOBAL_UNIT_ASSIGNED_CONTEXT((#12414,#12416,#12417))
REPRESENTATION_CONTEXT('','3D')
);
#12413=(
GEOMETRIC_REPRESENTATION_CONTEXT(3)
GLOBAL_UNCERTAINTY_ASSIGNED_CONTEXT((#12367))
GLOBAL_UNIT_ASSIGNED_CONTEXT((#12414,#12416,#12417))
REPRESENTATION_CONTEXT('','3D')
);
#12414=(
LENGTH_UNIT()
NAMED_UNIT(*)
SI_UNIT(.CENTI.,.METRE.)
);
#12416=(
NAMED_UNIT(*)
PLANE_ANGLE_UNIT()
SI_UNIT($,.RADIAN.)
);
#12417=(
NAMED_UNIT(*)
SI_UNIT($,.STERADIAN.)
SOLID_ANGLE_UNIT()
);
#12441=SHAPE_DEFINITION_REPRESENTATION(#12493,#12594);
#12493=PRODUCT_DEFINITION_SHAPE('',$,#12640);
#12594=SHAPE_REPRESENTATION('',(#7513),#12391);
#12616=PRODUCT_DEFINITION_CONTEXT('part definition',#12753,'design');
#12640=PRODUCT_DEFINITION('M4x30 stop screw','M4x30 stop screw',#12685,
#12616);
#12685=PRODUCT_DEFINITION_FORMATION('',$,#12778);
#12753=APPLICATION_CONTEXT(
'Core Data for Automotive Mechanical Design Process');
#12754=PRODUCT_CONTEXT('part definition',#12753,'mechanical');
#12778=PRODUCT('M4x30 stop screw','M4x30 stop screw','M4x30 stop screw',
(#12754));
#12870=COLOUR_RGB('Black',0.12,0.14,0.17);
#12871=FILL_AREA_STYLE_COLOUR('',#12870);
#12872=FILL_AREA_STYLE('',(#12871));
#12873=SURFACE_STYLE_FILL_AREA(#12872);
#12874=SURFACE_SIDE_STYLE('',(#12873));
#12875=SURFACE_STYLE_USAGE(.BOTH.,#12874);
#12876=PRESENTATION_STYLE_ASSIGNMENT((#12875));
ENDSEC;
END-ISO-10303-21;
